ISO-10303-21;
HEADER;
/* Generated by software containing ST-Developer
 * from STEP Tools, Inc. (www.steptools.com) 
 */

FILE_DESCRIPTION(
/* description */ ('XY cross-slide table'),
/* implementation_level */ '2;1');

FILE_NAME(
/* name */ 'Cap Screw - M4x16 (1).step',
/* time_stamp */ '2026-10-28T03:22:46-07:00',
/* author */ (''),
/* organization */ (''),
/* preprocessor_version */ 'ST-DEVELOPER v20.2',
/* originating_system */ 'Autodesk Translation Framework v15.17.0.0',
/* authorisation */ '');

FILE_SCHEMA (('AUTOMOTIVE_DESIGN { 1 0 10303 214 3 1 1 }'));
ENDSEC;

DATA;
#10=MECHANICAL_DESIGN_GEOMETRIC_PRESENTATION_REPRESENTATION('',(#1771),#62984);
#25=ORIENTED_CLOSED_SHELL('',*,#23072,.F.);
#34=BREP_WITH_VOIDS('Body1',#23071,(#25));
#1482=CONICAL_SURFACE('',#26057,0.325,0.785398163397448);
#1483=CONICAL_SURFACE('',#26061,0.335,0.785398163397448);
#1484=CONICAL_SURFACE('',#26065,0.21,0.463647609000806);
#1485=CONICAL_SURFACE('',#26069,0.18,0.785398163397448);
#1575=SHAPE_REPRESENTATION_RELATIONSHIP('SRR','None',#63434,#1658);
#1658=ADVANCED_BREP_SHAPE_REPRESENTATION('',(#34),#62971);
#1771=STYLED_ITEM('',(#63919),#34);
#2270=FACE_BOUND('',#5633,.T.);
#2787=PLANE('',#26055);
#2788=PLANE('',#26063);
#2789=PLANE('',#26071);
#2790=PLANE('',#26072);
#2791=PLANE('',#26073);
#2792=PLANE('',#26074);
#2793=PLANE('',#26075);
#2794=PLANE('',#26076);
#2795=PLANE('',#26077);
#2796=PLANE('',#26078);
#2797=PLANE('',#26079);
#3931=FACE_OUTER_BOUND('',#5628,.T.);
#3932=FACE_OUTER_BOUND('',#5629,.T.);
#3933=FACE_OUTER_BOUND('',#5630,.T.);
#3934=FACE_OUTER_BOUND('',#5631,.T.);
#3935=FACE_OUTER_BOUND('',#5632,.T.);
#3936=FACE_OUTER_BOUND('',#5634,.T.);
#3937=FACE_OUTER_BOUND('',#5635,.T.);
#3938=FACE_OUTER_BOUND('',#5636,.T.);
#3939=FACE_OUTER_BOUND('',#5637,.T.);
#3940=FACE_OUTER_BOUND('',#5638,.T.);
#3941=FACE_OUTER_BOUND('',#5639,.T.);
#3942=FACE_OUTER_BOUND('',#5640,.T.);
#3943=FACE_OUTER_BOUND('',#5641,.T.);
#3944=FACE_OUTER_BOUND('',#5642,.T.);
#3945=FACE_OUTER_BOUND('',#5643,.T.);
#3946=FACE_OUTER_BOUND('',#5644,.T.);
#3947=FACE_OUTER_BOUND('',#5645,.T.);
#5628=EDGE_LOOP('',(#19780));
#5629=EDGE_LOOP('',(#19781,#19782,#19783,#19784));
#5630=EDGE_LOOP('',(#19785,#19786,#19787,#19788));
#5631=EDGE_LOOP('',(#19789,#19790,#19791,#19792));
#5632=EDGE_LOOP('',(#19793));
#5633=EDGE_LOOP('',(#19794));
#5634=EDGE_LOOP('',(#19795,#19796,#19797,#19798));
#5635=EDGE_LOOP('',(#19799,#19800,#19801,#19802));
#5636=EDGE_LOOP('',(#19803,#19804,#19805,#19806));
#5637=EDGE_LOOP('',(#19807));
#5638=EDGE_LOOP('',(#19808,#19809,#19810,#19811));
#5639=EDGE_LOOP('',(#19812,#19813,#19814,#19815));
#5640=EDGE_LOOP('',(#19816,#19817,#19818,#19819));
#5641=EDGE_LOOP('',(#19820,#19821,#19822,#19823));
#5642=EDGE_LOOP('',(#19824,#19825,#19826,#19827));
#5643=EDGE_LOOP('',(#19828,#19829,#19830,#19831));
#5644=EDGE_LOOP('',(#19832,#19833,#19834,#19835,#19836,#19837));
#5645=EDGE_LOOP('',(#19838,#19839,#19840,#19841,#19842,#19843));
#7105=LINE('',#52468,#8592);
#7106=LINE('',#52472,#8593);
#7107=LINE('',#52476,#8594);
#7108=LINE('',#52483,#8595);
#7109=LINE('',#52487,#8596);
#7110=LINE('',#52491,#8597);
#7111=LINE('',#52496,#8598);
#7112=LINE('',#52498,#8599);
#7113=LINE('',#52500,#8600);
#7114=LINE('',#52501,#8601);
#7115=LINE('',#52504,#8602);
#7116=LINE('',#52506,#8603);
#7117=LINE('',#52507,#8604);
#7118=LINE('',#52510,#8605);
#7119=LINE('',#52512,#8606);
#7120=LINE('',#52513,#8607);
#7121=LINE('',#52516,#8608);
#7122=LINE('',#52518,#8609);
#7123=LINE('',#52519,#8610);
#7124=LINE('',#52522,#8611);
#7125=LINE('',#52524,#8612);
#7126=LINE('',#52525,#8613);
#7127=LINE('',#52527,#8614);
#7128=LINE('',#52528,#8615);
#8592=VECTOR('',#31778,0.325);
#8593=VECTOR('',#31783,0.35);
#8594=VECTOR('',#31788,0.335);
#8595=VECTOR('',#31797,0.21);
#8596=VECTOR('',#31802,0.2);
#8597=VECTOR('',#31807,0.18);
#8598=VECTOR('',#31812,1.);
#8599=VECTOR('',#31813,1.);
#8600=VECTOR('',#31814,1.);
#8601=VECTOR('',#31815,1.);
#8602=VECTOR('',#31818,1.);
#8603=VECTOR('',#31819,1.);
#8604=VECTOR('',#31820,1.);
#8605=VECTOR('',#31823,1.);
#8606=VECTOR('',#31824,1.);
#8607=VECTOR('',#31825,1.);
#8608=VECTOR('',#31828,1.);
#8609=VECTOR('',#31829,1.);
#8610=VECTOR('',#31830,1.);
#8611=VECTOR('',#31833,1.);
#8612=VECTOR('',#31834,1.);
#8613=VECTOR('',#31835,1.);
#8614=VECTOR('',#31838,1.);
#8615=VECTOR('',#31839,1.);
#9700=CIRCLE('',#26056,0.3);
#9701=CIRCLE('',#26058,0.35);
#9702=CIRCLE('',#26060,0.35);
#9703=CIRCLE('',#26062,0.32);
#9704=CIRCLE('',#26064,0.22);
#9705=CIRCLE('',#26066,0.1954);
#9706=CIRCLE('',#26068,0.1954);
#9707=CIRCLE('',#26070,0.16);
#11420=VERTEX_POINT('',#52463);
#11421=VERTEX_POINT('',#52466);
#11422=VERTEX_POINT('',#52470);
#11423=VERTEX_POINT('',#52474);
#11424=VERTEX_POINT('',#52478);
#11425=VERTEX_POINT('',#52481);
#11426=VERTEX_POINT('',#52485);
#11427=VERTEX_POINT('',#52489);
#11428=VERTEX_POINT('',#52494);
#11429=VERTEX_POINT('',#52495);
#11430=VERTEX_POINT('',#52497);
#11431=VERTEX_POINT('',#52499);
#11432=VERTEX_POINT('',#52503);
#11433=VERTEX_POINT('',#52505);
#11434=VERTEX_POINT('',#52509);
#11435=VERTEX_POINT('',#52511);
#11436=VERTEX_POINT('',#52515);
#11437=VERTEX_POINT('',#52517);
#11438=VERTEX_POINT('',#52521);
#11439=VERTEX_POINT('',#52523);
#14274=EDGE_CURVE('',#11420,#11420,#9700,.T.);
#14275=EDGE_CURVE('',#11421,#11421,#9701,.T.);
#14276=EDGE_CURVE('',#11421,#11420,#7105,.T.);
#14277=EDGE_CURVE('',#11422,#11422,#9702,.T.);
#14278=EDGE_CURVE('',#11422,#11421,#7106,.T.);
#14279=EDGE_CURVE('',#11423,#11423,#9703,.T.);
#14280=EDGE_CURVE('',#11423,#11422,#7107,.T.);
#14281=EDGE_CURVE('',#11424,#11424,#9704,.T.);
#14282=EDGE_CURVE('',#11425,#11425,#9705,.F.);
#14283=EDGE_CURVE('',#11425,#11424,#7108,.T.);
#14284=EDGE_CURVE('',#11426,#11426,#9706,.F.);
#14285=EDGE_CURVE('',#11426,#11425,#7109,.T.);
#14286=EDGE_CURVE('',#11427,#11427,#9707,.T.);
#14287=EDGE_CURVE('',#11427,#11426,#7110,.T.);
#14288=EDGE_CURVE('',#11428,#11429,#7111,.T.);
#14289=EDGE_CURVE('',#11429,#11430,#7112,.T.);
#14290=EDGE_CURVE('',#11430,#11431,#7113,.T.);
#14291=EDGE_CURVE('',#11428,#11431,#7114,.T.);
#14292=EDGE_CURVE('',#11429,#11432,#7115,.T.);
#14293=EDGE_CURVE('',#11432,#11433,#7116,.T.);
#14294=EDGE_CURVE('',#11433,#11430,#7117,.T.);
#14295=EDGE_CURVE('',#11432,#11434,#7118,.T.);
#14296=EDGE_CURVE('',#11434,#11435,#7119,.T.);
#14297=EDGE_CURVE('',#11435,#11433,#7120,.T.);
#14298=EDGE_CURVE('',#11434,#11436,#7121,.T.);
#14299=EDGE_CURVE('',#11436,#11437,#7122,.T.);
#14300=EDGE_CURVE('',#11437,#11435,#7123,.T.);
#14301=EDGE_CURVE('',#11436,#11438,#7124,.T.);
#14302=EDGE_CURVE('',#11438,#11439,#7125,.T.);
#14303=EDGE_CURVE('',#11439,#11437,#7126,.T.);
#14304=EDGE_CURVE('',#11438,#11428,#7127,.T.);
#14305=EDGE_CURVE('',#11431,#11439,#7128,.T.);
#19780=ORIENTED_EDGE('',*,*,#14274,.F.);
#19781=ORIENTED_EDGE('',*,*,#14275,.F.);
#19782=ORIENTED_EDGE('',*,*,#14276,.T.);
#19783=ORIENTED_EDGE('',*,*,#14274,.T.);
#19784=ORIENTED_EDGE('',*,*,#14276,.F.);
#19785=ORIENTED_EDGE('',*,*,#14277,.F.);
#19786=ORIENTED_EDGE('',*,*,#14278,.T.);
#19787=ORIENTED_EDGE('',*,*,#14275,.T.);
#19788=ORIENTED_EDGE('',*,*,#14278,.F.);
#19789=ORIENTED_EDGE('',*,*,#14279,.F.);
#19790=ORIENTED_EDGE('',*,*,#14280,.T.);
#19791=ORIENTED_EDGE('',*,*,#14277,.T.);
#19792=ORIENTED_EDGE('',*,*,#14280,.F.);
#19793=ORIENTED_EDGE('',*,*,#14279,.T.);
#19794=ORIENTED_EDGE('',*,*,#14281,.F.);
#19795=ORIENTED_EDGE('',*,*,#14282,.F.);
#19796=ORIENTED_EDGE('',*,*,#14283,.T.);
#19797=ORIENTED_EDGE('',*,*,#14281,.T.);
#19798=ORIENTED_EDGE('',*,*,#14283,.F.);
#19799=ORIENTED_EDGE('',*,*,#14284,.F.);
#19800=ORIENTED_EDGE('',*,*,#14285,.T.);
#19801=ORIENTED_EDGE('',*,*,#14282,.T.);
#19802=ORIENTED_EDGE('',*,*,#14285,.F.);
#19803=ORIENTED_EDGE('',*,*,#14286,.F.);
#19804=ORIENTED_EDGE('',*,*,#14287,.T.);
#19805=ORIENTED_EDGE('',*,*,#14284,.T.);
#19806=ORIENTED_EDGE('',*,*,#14287,.F.);
#19807=ORIENTED_EDGE('',*,*,#14286,.T.);
#19808=ORIENTED_EDGE('',*,*,#14288,.T.);
#19809=ORIENTED_EDGE('',*,*,#14289,.T.);
#19810=ORIENTED_EDGE('',*,*,#14290,.T.);
#19811=ORIENTED_EDGE('',*,*,#14291,.F.);
#19812=ORIENTED_EDGE('',*,*,#14292,.T.);
#19813=ORIENTED_EDGE('',*,*,#14293,.T.);
#19814=ORIENTED_EDGE('',*,*,#14294,.T.);
#19815=ORIENTED_EDGE('',*,*,#14289,.F.);
#19816=ORIENTED_EDGE('',*,*,#14295,.T.);
#19817=ORIENTED_EDGE('',*,*,#14296,.T.);
#19818=ORIENTED_EDGE('',*,*,#14297,.T.);
#19819=ORIENTED_EDGE('',*,*,#14293,.F.);
#19820=ORIENTED_EDGE('',*,*,#14298,.T.);
#19821=ORIENTED_EDGE('',*,*,#14299,.T.);
#19822=ORIENTED_EDGE('',*,*,#14300,.T.);
#19823=ORIENTED_EDGE('',*,*,#14296,.F.);
#19824=ORIENTED_EDGE('',*,*,#14301,.T.);
#19825=ORIENTED_EDGE('',*,*,#14302,.T.);
#19826=ORIENTED_EDGE('',*,*,#14303,.T.);
#19827=ORIENTED_EDGE('',*,*,#14299,.F.);
#19828=ORIENTED_EDGE('',*,*,#14304,.T.);
#19829=ORIENTED_EDGE('',*,*,#14291,.T.);
#19830=ORIENTED_EDGE('',*,*,#14305,.T.);
#19831=ORIENTED_EDGE('',*,*,#14302,.F.);
#19832=ORIENTED_EDGE('',*,*,#14304,.F.);
#19833=ORIENTED_EDGE('',*,*,#14301,.F.);
#19834=ORIENTED_EDGE('',*,*,#14298,.F.);
#19835=ORIENTED_EDGE('',*,*,#14295,.F.);
#19836=ORIENTED_EDGE('',*,*,#14292,.F.);
#19837=ORIENTED_EDGE('',*,*,#14288,.F.);
#19838=ORIENTED_EDGE('',*,*,#14305,.F.);
#19839=ORIENTED_EDGE('',*,*,#14290,.F.);
#19840=ORIENTED_EDGE('',*,*,#14294,.F.);
#19841=ORIENTED_EDGE('',*,*,#14297,.F.);
#19842=ORIENTED_EDGE('',*,*,#14300,.F.);
#19843=ORIENTED_EDGE('',*,*,#14303,.F.);
#21496=CYLINDRICAL_SURFACE('',#26059,0.35);
#21497=CYLINDRICAL_SURFACE('',#26067,0.1954);
#22712=ADVANCED_FACE('',(#3931),#2787,.T.);
#22713=ADVANCED_FACE('',(#3932),#1482,.T.);
#22714=ADVANCED_FACE('',(#3933),#21496,.T.);
#22715=ADVANCED_FACE('',(#3934),#1483,.T.);
#22716=ADVANCED_FACE('',(#3935,#2270),#2788,.T.);
#22717=ADVANCED_FACE('',(#3936),#1484,.T.);
#22718=ADVANCED_FACE('',(#3937),#21497,.T.);
#22719=ADVANCED_FACE('',(#3938),#1485,.T.);
#22720=ADVANCED_FACE('',(#3939),#2789,.T.);
#22721=ADVANCED_FACE('',(#3940),#2790,.F.);
#22722=ADVANCED_FACE('',(#3941),#2791,.F.);
#22723=ADVANCED_FACE('',(#3942),#2792,.F.);
#22724=ADVANCED_FACE('',(#3943),#2793,.F.);
#22725=ADVANCED_FACE('',(#3944),#2794,.F.);
#22726=ADVANCED_FACE('',(#3945),#2795,.F.);
#22727=ADVANCED_FACE('',(#3946),#2796,.F.);
#22728=ADVANCED_FACE('',(#3947),#2797,.F.);
#23071=CLOSED_SHELL('',(#22712,#22713,#22714,#22715,#22716,#22717,#22718,
#22719,#22720));
#23072=CLOSED_SHELL('',(#22721,#22722,#22723,#22724,#22725,#22726,#22727,
#22728));
#26054=AXIS2_PLACEMENT_3D('',#52461,#31768,#31769);
#26055=AXIS2_PLACEMENT_3D('',#52462,#31770,#31771);
#26056=AXIS2_PLACEMENT_3D('',#52464,#31772,#31773);
#26057=AXIS2_PLACEMENT_3D('',#52465,#31774,#31775);
#26058=AXIS2_PLACEMENT_3D('',#52467,#31776,#31777);
#26059=AXIS2_PLACEMENT_3D('',#52469,#31779,#31780);
#26060=AXIS2_PLACEMENT_3D('',#52471,#31781,#31782);
#26061=AXIS2_PLACEMENT_3D('',#52473,#31784,#31785);
#26062=AXIS2_PLACEMENT_3D('',#52475,#31786,#31787);
#26063=AXIS2_PLACEMENT_3D('',#52477,#31789,#31790);
#26064=AXIS2_PLACEMENT_3D('',#52479,#31791,#31792);
#26065=AXIS2_PLACEMENT_3D('',#52480,#31793,#31794);
#26066=AXIS2_PLACEMENT_3D('',#52482,#31795,#31796);
#26067=AXIS2_PLACEMENT_3D('',#52484,#31798,#31799);
#26068=AXIS2_PLACEMENT_3D('',#52486,#31800,#31801);
#26069=AXIS2_PLACEMENT_3D('',#52488,#31803,#31804);
#26070=AXIS2_PLACEMENT_3D('',#52490,#31805,#31806);
#26071=AXIS2_PLACEMENT_3D('',#52492,#31808,#31809);
#26072=AXIS2_PLACEMENT_3D('',#52493,#31810,#31811);
#26073=AXIS2_PLACEMENT_3D('',#52502,#31816,#31817);
#26074=AXIS2_PLACEMENT_3D('',#52508,#31821,#31822);
#26075=AXIS2_PLACEMENT_3D('',#52514,#31826,#31827);
#26076=AXIS2_PLACEMENT_3D('',#52520,#31831,#31832);
#26077=AXIS2_PLACEMENT_3D('',#52526,#31836,#31837);
#26078=AXIS2_PLACEMENT_3D('',#52529,#31840,#31841);
#26079=AXIS2_PLACEMENT_3D('',#52530,#31842,#31843);
#31768=DIRECTION('axis',(0.,0.,1.));
#31769=DIRECTION('refdir',(1.,0.,0.));
#31770=DIRECTION('center_axis',(0.,1.,0.));
#31771=DIRECTION('ref_axis',(0.,0.,1.));
#31772=DIRECTION('center_axis',(0.,-1.,0.));
#31773=DIRECTION('ref_axis',(1.,0.,0.));
#31774=DIRECTION('center_axis',(0.,-1.,0.));
#31775=DIRECTION('ref_axis',(1.,0.,0.));
#31776=DIRECTION('center_axis',(0.,-1.,0.));
#31777=DIRECTION('ref_axis',(1.,0.,0.));
#31778=DIRECTION('',(0.707106781186547,0.707106781186548,8.65956056235493E-17));
#31779=DIRECTION('center_axis',(0.,-1.,0.));
#31780=DIRECTION('ref_axis',(1.,0.,0.));
#31781=DIRECTION('center_axis',(0.,-1.,0.));
#31782=DIRECTION('ref_axis',(1.,0.,0.));
#31783=DIRECTION('',(0.,1.,0.));
#31784=DIRECTION('center_axis',(0.,1.,0.));
#31785=DIRECTION('ref_axis',(1.,0.,0.));
#31786=DIRECTION('center_axis',(0.,-1.,0.));
#31787=DIRECTION('ref_axis',(1.,0.,0.));
#31788=DIRECTION('',(-0.707106781186547,0.707106781186548,-8.65956056235493E-17));
#31789=DIRECTION('center_axis',(0.,-1.,0.));
#31790=DIRECTION('ref_axis',(0.,0.,-1.));
#31791=DIRECTION('center_axis',(0.,-1.,0.));
#31792=DIRECTION('ref_axis',(1.,0.,0.));
#31793=DIRECTION('center_axis',(0.,1.,0.));
#31794=DIRECTION('ref_axis',(1.,0.,0.));
#31795=DIRECTION('center_axis',(0.,1.,0.));
#31796=DIRECTION('ref_axis',(1.,0.,0.));
#31797=DIRECTION('',(-0.447213595499958,0.894427190999916,-5.47678698264203E-17));
#31798=DIRECTION('center_axis',(0.,-1.,0.));
#31799=DIRECTION('ref_axis',(1.,0.,0.));
#31800=DIRECTION('center_axis',(0.,1.,0.));
#31801=DIRECTION('ref_axis',(1.,0.,0.));
#31802=DIRECTION('',(0.,1.,0.));
#31803=DIRECTION('center_axis',(0.,1.,0.));
#31804=DIRECTION('ref_axis',(1.,0.,0.));
#31805=DIRECTION('center_axis',(0.,-1.,0.));
#31806=DIRECTION('ref_axis',(1.,0.,0.));
#31807=DIRECTION('',(-0.707106781186547,0.707106781186548,-8.65956056235493E-17));
#31808=DIRECTION('center_axis',(0.,-1.,0.));
#31809=DIRECTION('ref_axis',(0.,0.,-1.));
#31810=DIRECTION('center_axis',(0.866025403784439,0.,-0.5));
#31811=DIRECTION('ref_axis',(0.5,0.,0.866025403784439));
#31812=DIRECTION('',(-0.5,0.,-0.866025403784439));
#31813=DIRECTION('',(0.,-1.,0.));
#31814=DIRECTION('',(0.5,0.,0.866025403784439));
#31815=DIRECTION('',(0.,-1.,0.));
#31816=DIRECTION('center_axis',(1.60246890531964E-16,0.,-1.));
#31817=DIRECTION('ref_axis',(1.,0.,1.60246890531964E-16));
#31818=DIRECTION('',(-1.,0.,-1.60246890531964E-16));
#31819=DIRECTION('',(0.,-1.,0.));
#31820=DIRECTION('',(1.,0.,1.60246890531964E-16));
#31821=DIRECTION('center_axis',(-0.866025403784439,0.,-0.5));
#31822=DIRECTION('ref_axis',(0.5,0.,-0.866025403784439));
#31823=DIRECTION('',(-0.5,0.,0.866025403784439));
#31824=DIRECTION('',(0.,-1.,0.));
#31825=DIRECTION('',(0.5,0.,-0.866025403784439));
#31826=DIRECTION('center_axis',(-0.866025403784439,0.,0.5));
#31827=DIRECTION('ref_axis',(-0.5,0.,-0.866025403784439));
#31828=DIRECTION('',(0.5,0.,0.866025403784439));
#31829=DIRECTION('',(0.,-1.,0.));
#31830=DIRECTION('',(-0.5,0.,-0.866025403784439));
#31831=DIRECTION('center_axis',(-1.60246890531964E-16,0.,1.));
#31832=DIRECTION('ref_axis',(-1.,0.,-1.60246890531964E-16));
#31833=DIRECTION('',(1.,0.,1.60246890531964E-16));
#31834=DIRECTION('',(0.,-1.,0.));
#31835=DIRECTION('',(-1.,0.,-1.60246890531964E-16));
#31836=DIRECTION('center_axis',(0.866025403784439,0.,0.5));
#31837=DIRECTION('ref_axis',(-0.5,0.,0.866025403784439));
#31838=DIRECTION('',(0.5,0.,-0.866025403784439));
#31839=DIRECTION('',(-0.5,0.,0.866025403784439));
#31840=DIRECTION('center_axis',(0.,1.,0.));
#31841=DIRECTION('ref_axis',(1.,0.,0.));
#31842=DIRECTION('center_axis',(0.,-1.,0.));
#31843=DIRECTION('ref_axis',(0.,0.,-1.));
#52461=CARTESIAN_POINT('',(0.,0.,0.));
#52462=CARTESIAN_POINT('Origin',(0.3,0.4,0.));
#52463=CARTESIAN_POINT('',(-0.3,0.4,-3.67394039744206E-17));
#52464=CARTESIAN_POINT('Origin',(0.,0.4,0.));
#52465=CARTESIAN_POINT('Origin',(0.,0.375,0.));
#52466=CARTESIAN_POINT('',(-0.35,0.35,-4.28626379701573E-17));
#52467=CARTESIAN_POINT('Origin',(0.,0.35,0.));
#52468=CARTESIAN_POINT('',(-0.325,0.375,-3.9801020972289E-17));
#52469=CARTESIAN_POINT('Origin',(0.,0.19,0.));
#52470=CARTESIAN_POINT('',(-0.35,0.03,-4.28626379701574E-17));
#52471=CARTESIAN_POINT('Origin',(0.,0.03,0.));
#52472=CARTESIAN_POINT('',(-0.35,0.19,-4.28626379701574E-17));
#52473=CARTESIAN_POINT('Origin',(0.,0.0149999999999999,0.));
#52474=CARTESIAN_POINT('',(-0.32,-3.29597460435593E-17,-3.91886975727153E-17));
#52475=CARTESIAN_POINT('Origin',(0.,0.,0.));
#52476=CARTESIAN_POINT('',(-0.335,0.0149999999999999,-4.10256677714363E-17));
#52477=CARTESIAN_POINT('Origin',(0.22,0.,0.));
#52478=CARTESIAN_POINT('',(-0.22,-6.93889390390723E-18,-2.69422295812418E-17));
#52479=CARTESIAN_POINT('Origin',(0.,0.,0.));
#52480=CARTESIAN_POINT('Origin',(0.,-0.02,0.));
#52481=CARTESIAN_POINT('',(-0.1954,-0.0492,2.39295984553393E-17));
#52482=CARTESIAN_POINT('Origin',(0.,-0.0492,0.));
#52483=CARTESIAN_POINT('',(-0.21,-0.02,-2.57175827820944E-17));
#52484=CARTESIAN_POINT('Origin',(0.,-0.8,0.));
#52485=CARTESIAN_POINT('',(-0.1954,-1.5646,2.39295984553393E-17));
#52486=CARTESIAN_POINT('Origin',(0.,-1.5646,0.));
#52487=CARTESIAN_POINT('',(-0.1954,-0.8,-2.39295984553393E-17));
#52488=CARTESIAN_POINT('Origin',(0.,-1.58,0.));
#52489=CARTESIAN_POINT('',(-0.16,-1.6,-1.95943487863577E-17));
#52490=CARTESIAN_POINT('Origin',(0.,-1.6,0.));
#52491=CARTESIAN_POINT('',(-0.18,-1.58,-2.20436423846524E-17));
#52492=CARTESIAN_POINT('Origin',(0.,-1.6,0.));
#52493=CARTESIAN_POINT('Origin',(0.0866025403784439,-0.4,-0.15));
#52494=CARTESIAN_POINT('',(0.173205080756888,-0.4,0.));
#52495=CARTESIAN_POINT('',(0.0866025403784439,-0.4,-0.15));
#52496=CARTESIAN_POINT('',(0.173205080756888,-0.4,0.));
#52497=CARTESIAN_POINT('',(0.0866025403784439,-0.64,-0.15));
#52498=CARTESIAN_POINT('',(0.0866025403784439,-0.4,-0.15));
#52499=CARTESIAN_POINT('',(0.173205080756888,-0.64,0.));
#52500=CARTESIAN_POINT('',(0.173205080756888,-0.64,0.));
#52501=CARTESIAN_POINT('',(0.173205080756888,-0.4,0.));
#52502=CARTESIAN_POINT('Origin',(-0.0866025403784438,-0.4,-0.15));
#52503=CARTESIAN_POINT('',(-0.0866025403784438,-0.4,-0.15));
#52504=CARTESIAN_POINT('',(0.0866025403784439,-0.4,-0.15));
#52505=CARTESIAN_POINT('',(-0.0866025403784438,-0.64,-0.15));
#52506=CARTESIAN_POINT('',(-0.0866025403784438,-0.4,-0.15));
#52507=CARTESIAN_POINT('',(0.0866025403784439,-0.64,-0.15));
#52508=CARTESIAN_POINT('Origin',(-0.173205080756888,-0.4,-2.77555756156289E-17));
#52509=CARTESIAN_POINT('',(-0.173205080756888,-0.4,-2.12115047744981E-17));
#52510=CARTESIAN_POINT('',(-0.0866025403784438,-0.4,-0.15));
#52511=CARTESIAN_POINT('',(-0.173205080756888,-0.64,-2.77555756156289E-17));
#52512=CARTESIAN_POINT('',(-0.173205080756888,-0.4,-2.12115047744981E-17));
#52513=CARTESIAN_POINT('',(-0.0866025403784438,-0.64,-0.15));
#52514=CARTESIAN_POINT('Origin',(-0.0866025403784439,-0.4,0.15));
#52515=CARTESIAN_POINT('',(-0.0866025403784439,-0.4,0.15));
#52516=CARTESIAN_POINT('',(-0.173205080756888,-0.4,-2.12115047744981E-17));
#52517=CARTESIAN_POINT('',(-0.0866025403784439,-0.64,0.15));
#52518=CARTESIAN_POINT('',(-0.0866025403784439,-0.4,0.15));
#52519=CARTESIAN_POINT('',(-0.173205080756888,-0.64,-2.12115047744981E-17));
#52520=CARTESIAN_POINT('Origin',(0.0866025403784439,-0.4,0.15));
#52521=CARTESIAN_POINT('',(0.0866025403784439,-0.4,0.15));
#52522=CARTESIAN_POINT('',(-0.0866025403784439,-0.4,0.15));
#52523=CARTESIAN_POINT('',(0.0866025403784439,-0.64,0.15));
#52524=CARTESIAN_POINT('',(0.0866025403784439,-0.4,0.15));
#52525=CARTESIAN_POINT('',(-0.0866025403784439,-0.64,0.15));
#52526=CARTESIAN_POINT('Origin',(0.173205080756888,-0.4,0.));
#52527=CARTESIAN_POINT('',(0.0866025403784439,-0.4,0.15));
#52528=CARTESIAN_POINT('',(0.0866025403784439,-0.64,0.15));
#52529=CARTESIAN_POINT('Origin',(0.,-0.4,-2.77555756156289E-17));
#52530=CARTESIAN_POINT('Origin',(0.,-0.64,-2.77555756156289E-17));
#62872=UNCERTAINTY_MEASURE_WITH_UNIT(LENGTH_MEASURE(0.001),#62985,
'DISTANCE_ACCURACY_VALUE',
'Maximum model space distance between geometric entities at asserted c
onnectivities');
#62885=UNCERTAINTY_MEASURE_WITH_UNIT(LENGTH_MEASURE(0.001),#62985,
'DISTANCE_ACCURACY_VALUE',
'Maximum model space distance between geometric entities at asserted c
onnectivities');
#62971=(
GEOMETRIC_REPRESENTATION_CONTEXT(3)
GLOBAL_UNCERTAINTY_ASSIGNED_CONTEXT((#62872))
GLOBAL_UNIT_ASSIGNED_CONTEXT((#62985,#62987,#62988))
REPRESENTATION_CONTEXT('','3D')
);
#62984=(
GEOMETRIC_REPRESENTATION_CONTEXT(3)
GLOBAL_UNCERTAINTY_ASSIGNED_CONTEXT((#62885))
GLOBAL_UNIT_ASSIGNED_CONTEXT((#62985,#62987,#62988))
REPRESENTATION_CONTEXT('','3D')
);
#62985=(
LENGTH_UNIT()
NAMED_UNIT(*)
SI_UNIT(.CENTI.,.METRE.)
);
#62987=(
NAMED_UNIT(*)
PLANE_ANGLE_UNIT()
SI_UNIT($,.RADIAN.)
);
#62988=(
NAMED_UNIT(*)
SI_UNIT($,.STERADIAN.)
SOLID_ANGLE_UNIT()
);
#63074=SHAPE_DEFINITION_REPRESENTATION(#63265,#63434);
#63265=PRODUCT_DEFINITION_SHAPE('',$,#63533);
#63434=SHAPE_REPRESENTATION('',(#26054),#62971);
#63447=PRODUCT_DEFINITION_CONTEXT('part definition',#63743,'design');
#63533=PRODUCT_DEFINITION('Cap Screw - M4x16 (1)','Cap Screw - M4x16 (1)',
#63631,#63447);
#63631=PRODUCT_DEFINITION_FORMATION('',$,#63830);
#63743=APPLICATION_CONTEXT(
'Core Data for Automotive Mechanical Design Process');
#63744=PRODUCT_CONTEXT('part definition',#63743,'mechanical');
#63830=PRODUCT('Cap Screw - M4x16 (1)','Cap Screw - M4x16 (1)',
'Cap Screw - M4x16 (1)',(#63744));
#63913=COLOUR_RGB('Black',0.12,0.14,0.17);
#63914=FILL_AREA_STYLE_COLOUR('',#63913);
#63915=FILL_AREA_STYLE('',(#63914));
#63916=SURFACE_STYLE_FILL_AREA(#63915);
#63917=SURFACE_SIDE_STYLE('',(#63916));
#63918=SURFACE_STYLE_USAGE(.BOTH.,#63917);
#63919=PRESENTATION_STYLE_ASSIGNMENT((#63918));
ENDSEC;
END-ISO-10303-21;
